ISO-10303-21;
HEADER;
/* Generated by software containing ST-Developer
 * from STEP Tools, Inc. (www.steptools.com) 
 */

FILE_DESCRIPTION(
/* description */ ('XY cross-slide table'),
/* implementation_level */ '2;1');

FILE_NAME(
/* name */ 'Cap Screw - M6x25 (1).step',
/* time_stamp */ '2026-10-28T03:22:46-07:00',
/* author */ (''),
/* organization */ (''),
/* preprocessor_version */ 'ST-DEVELOPER v20.2',
/* originating_system */ 'Autodesk Translation Framework v15.17.0.0',
/* authorisation */ '');

FILE_SCHEMA (('AUTOMOTIVE_DESIGN { 1 0 10303 214 3 1 1 }'));
ENDSEC;

DATA;
#10=MECHANICAL_DESIGN_GEOMETRIC_PRESENTATION_REPRESENTATION('',(#1782),#62984);
#27=ORIENTED_CLOSED_SHELL('',*,#23085,.F.);
#36=BREP_WITH_VOIDS('Body1',#23084,(#27));
#1492=CONICAL_SURFACE('',#26387,0.475,0.785398163397449);
#1493=CONICAL_SURFACE('',#26391,0.485,0.785398163397448);
#1494=CONICAL_SURFACE('',#26395,0.31,0.463647609000806);
#1495=CONICAL_SURFACE('',#26399,0.27,0.785398163397448);
#1586=SHAPE_REPRESENTATION_RELATIONSHIP('SRR','None',#63446,#1669);
#1669=ADVANCED_BREP_SHAPE_REPRESENTATION('',(#36),#62983);
#1782=STYLED_ITEM('',(#63919),#36);
#2295=FACE_BOUND('',#5893,.T.);
#2858=PLANE('',#26385);
#2859=PLANE('',#26393);
#2860=PLANE('',#26401);
#2861=PLANE('',#26402);
#2862=PLANE('',#26403);
#2863=PLANE('',#26404);
#2864=PLANE('',#26405);
#2865=PLANE('',#26406);
#2866=PLANE('',#26407);
#2867=PLANE('',#26408);
#2868=PLANE('',#26409);
#4166=FACE_OUTER_BOUND('',#5888,.T.);
#4167=FACE_OUTER_BOUND('',#5889,.T.);
#4168=FACE_OUTER_BOUND('',#5890,.T.);
#4169=FACE_OUTER_BOUND('',#5891,.T.);
#4170=FACE_OUTER_BOUND('',#5892,.T.);
#4171=FACE_OUTER_BOUND('',#5894,.T.);
#4172=FACE_OUTER_BOUND('',#5895,.T.);
#4173=FACE_OUTER_BOUND('',#5896,.T.);
#4174=FACE_OUTER_BOUND('',#5897,.T.);
#4175=FACE_OUTER_BOUND('',#5898,.T.);
#4176=FACE_OUTER_BOUND('',#5899,.T.);
#4177=FACE_OUTER_BOUND('',#5900,.T.);
#4178=FACE_OUTER_BOUND('',#5901,.T.);
#4179=FACE_OUTER_BOUND('',#5902,.T.);
#4180=FACE_OUTER_BOUND('',#5903,.T.);
#4181=FACE_OUTER_BOUND('',#5904,.T.);
#4182=FACE_OUTER_BOUND('',#5905,.T.);
#5888=EDGE_LOOP('',(#20976));
#5889=EDGE_LOOP('',(#20977,#20978,#20979,#20980));
#5890=EDGE_LOOP('',(#20981,#20982,#20983,#20984));
#5891=EDGE_LOOP('',(#20985,#20986,#20987,#20988));
#5892=EDGE_LOOP('',(#20989));
#5893=EDGE_LOOP('',(#20990));
#5894=EDGE_LOOP('',(#20991,#20992,#20993,#20994));
#5895=EDGE_LOOP('',(#20995,#20996,#20997,#20998));
#5896=EDGE_LOOP('',(#20999,#21000,#21001,#21002));
#5897=EDGE_LOOP('',(#21003));
#5898=EDGE_LOOP('',(#21004,#21005,#21006,#21007));
#5899=EDGE_LOOP('',(#21008,#21009,#21010,#21011));
#5900=EDGE_LOOP('',(#21012,#21013,#21014,#21015));
#5901=EDGE_LOOP('',(#21016,#21017,#21018,#21019));
#5902=EDGE_LOOP('',(#21020,#21021,#21022,#21023));
#5903=EDGE_LOOP('',(#21024,#21025,#21026,#21027));
#5904=EDGE_LOOP('',(#21028,#21029,#21030,#21031,#21032,#21033));
#5905=EDGE_LOOP('',(#21034,#21035,#21036,#21037,#21038,#21039));
#7369=LINE('',#62673,#8856);
#7370=LINE('',#62677,#8857);
#7371=LINE('',#62681,#8858);
#7372=LINE('',#62688,#8859);
#7373=LINE('',#62692,#8860);
#7374=LINE('',#62696,#8861);
#7375=LINE('',#62701,#8862);
#7376=LINE('',#62703,#8863);
#7377=LINE('',#62705,#8864);
#7378=LINE('',#62706,#8865);
#7379=LINE('',#62709,#8866);
#7380=LINE('',#62711,#8867);
#7381=LINE('',#62712,#8868);
#7382=LINE('',#62715,#8869);
#7383=LINE('',#62717,#8870);
#7384=LINE('',#62718,#8871);
#7385=LINE('',#62721,#8872);
#7386=LINE('',#62723,#8873);
#7387=LINE('',#62724,#8874);
#7388=LINE('',#62727,#8875);
#7389=LINE('',#62729,#8876);
#7390=LINE('',#62730,#8877);
#7391=LINE('',#62732,#8878);
#7392=LINE('',#62733,#8879);
#8856=VECTOR('',#32702,0.475);
#8857=VECTOR('',#32707,0.5);
#8858=VECTOR('',#32712,0.485);
#8859=VECTOR('',#32721,0.31);
#8860=VECTOR('',#32726,0.3);
#8861=VECTOR('',#32731,0.27);
#8862=VECTOR('',#32736,1.);
#8863=VECTOR('',#32737,1.);
#8864=VECTOR('',#32738,1.);
#8865=VECTOR('',#32739,1.);
#8866=VECTOR('',#32742,1.);
#8867=VECTOR('',#32743,1.);
#8868=VECTOR('',#32744,1.);
#8869=VECTOR('',#32747,1.);
#8870=VECTOR('',#32748,1.);
#8871=VECTOR('',#32749,1.);
#8872=VECTOR('',#32752,1.);
#8873=VECTOR('',#32753,1.);
#8874=VECTOR('',#32754,1.);
#8875=VECTOR('',#32757,1.);
#8876=VECTOR('',#32758,1.);
#8877=VECTOR('',#32759,1.);
#8878=VECTOR('',#32762,1.);
#8879=VECTOR('',#32763,1.);
#9765=CIRCLE('',#26386,0.45);
#9766=CIRCLE('',#26388,0.5);
#9767=CIRCLE('',#26390,0.5);
#9768=CIRCLE('',#26392,0.47);
#9769=CIRCLE('',#26394,0.32);
#9770=CIRCLE('',#26396,0.2942);
#9771=CIRCLE('',#26398,0.2942);
#9772=CIRCLE('',#26400,0.24);
#11816=VERTEX_POINT('',#62668);
#11817=VERTEX_POINT('',#62671);
#11818=VERTEX_POINT('',#62675);
#11819=VERTEX_POINT('',#62679);
#11820=VERTEX_POINT('',#62683);
#11821=VERTEX_POINT('',#62686);
#11822=VERTEX_POINT('',#62690);
#11823=VERTEX_POINT('',#62694);
#11824=VERTEX_POINT('',#62699);
#11825=VERTEX_POINT('',#62700);
#11826=VERTEX_POINT('',#62702);
#11827=VERTEX_POINT('',#62704);
#11828=VERTEX_POINT('',#62708);
#11829=VERTEX_POINT('',#62710);
#11830=VERTEX_POINT('',#62714);
#11831=VERTEX_POINT('',#62716);
#11832=VERTEX_POINT('',#62720);
#11833=VERTEX_POINT('',#62722);
#11834=VERTEX_POINT('',#62726);
#11835=VERTEX_POINT('',#62728);
#14872=EDGE_CURVE('',#11816,#11816,#9765,.T.);
#14873=EDGE_CURVE('',#11817,#11817,#9766,.T.);
#14874=EDGE_CURVE('',#11817,#11816,#7369,.T.);
#14875=EDGE_CURVE('',#11818,#11818,#9767,.T.);
#14876=EDGE_CURVE('',#11818,#11817,#7370,.T.);
#14877=EDGE_CURVE('',#11819,#11819,#9768,.T.);
#14878=EDGE_CURVE('',#11819,#11818,#7371,.T.);
#14879=EDGE_CURVE('',#11820,#11820,#9769,.T.);
#14880=EDGE_CURVE('',#11821,#11821,#9770,.F.);
#14881=EDGE_CURVE('',#11821,#11820,#7372,.T.);
#14882=EDGE_CURVE('',#11822,#11822,#9771,.F.);
#14883=EDGE_CURVE('',#11822,#11821,#7373,.T.);
#14884=EDGE_CURVE('',#11823,#11823,#9772,.T.);
#14885=EDGE_CURVE('',#11823,#11822,#7374,.T.);
#14886=EDGE_CURVE('',#11824,#11825,#7375,.T.);
#14887=EDGE_CURVE('',#11825,#11826,#7376,.T.);
#14888=EDGE_CURVE('',#11826,#11827,#7377,.T.);
#14889=EDGE_CURVE('',#11824,#11827,#7378,.T.);
#14890=EDGE_CURVE('',#11825,#11828,#7379,.T.);
#14891=EDGE_CURVE('',#11828,#11829,#7380,.T.);
#14892=EDGE_CURVE('',#11829,#11826,#7381,.T.);
#14893=EDGE_CURVE('',#11828,#11830,#7382,.T.);
#14894=EDGE_CURVE('',#11830,#11831,#7383,.T.);
#14895=EDGE_CURVE('',#11831,#11829,#7384,.T.);
#14896=EDGE_CURVE('',#11830,#11832,#7385,.T.);
#14897=EDGE_CURVE('',#11832,#11833,#7386,.T.);
#14898=EDGE_CURVE('',#11833,#11831,#7387,.T.);
#14899=EDGE_CURVE('',#11832,#11834,#7388,.T.);
#14900=EDGE_CURVE('',#11834,#11835,#7389,.T.);
#14901=EDGE_CURVE('',#11835,#11833,#7390,.T.);
#14902=EDGE_CURVE('',#11834,#11824,#7391,.T.);
#14903=EDGE_CURVE('',#11827,#11835,#7392,.T.);
#20976=ORIENTED_EDGE('',*,*,#14872,.F.);
#20977=ORIENTED_EDGE('',*,*,#14873,.F.);
#20978=ORIENTED_EDGE('',*,*,#14874,.T.);
#20979=ORIENTED_EDGE('',*,*,#14872,.T.);
#20980=ORIENTED_EDGE('',*,*,#14874,.F.);
#20981=ORIENTED_EDGE('',*,*,#14875,.F.);
#20982=ORIENTED_EDGE('',*,*,#14876,.T.);
#20983=ORIENTED_EDGE('',*,*,#14873,.T.);
#20984=ORIENTED_EDGE('',*,*,#14876,.F.);
#20985=ORIENTED_EDGE('',*,*,#14877,.F.);
#20986=ORIENTED_EDGE('',*,*,#14878,.T.);
#20987=ORIENTED_EDGE('',*,*,#14875,.T.);
#20988=ORIENTED_EDGE('',*,*,#14878,.F.);
#20989=ORIENTED_EDGE('',*,*,#14877,.T.);
#20990=ORIENTED_EDGE('',*,*,#14879,.F.);
#20991=ORIENTED_EDGE('',*,*,#14880,.F.);
#20992=ORIENTED_EDGE('',*,*,#14881,.T.);
#20993=ORIENTED_EDGE('',*,*,#14879,.T.);
#20994=ORIENTED_EDGE('',*,*,#14881,.F.);
#20995=ORIENTED_EDGE('',*,*,#14882,.F.);
#20996=ORIENTED_EDGE('',*,*,#14883,.T.);
#20997=ORIENTED_EDGE('',*,*,#14880,.T.);
#20998=ORIENTED_EDGE('',*,*,#14883,.F.);
#20999=ORIENTED_EDGE('',*,*,#14884,.F.);
#21000=ORIENTED_EDGE('',*,*,#14885,.T.);
#21001=ORIENTED_EDGE('',*,*,#14882,.T.);
#21002=ORIENTED_EDGE('',*,*,#14885,.F.);
#21003=ORIENTED_EDGE('',*,*,#14884,.T.);
#21004=ORIENTED_EDGE('',*,*,#14886,.T.);
#21005=ORIENTED_EDGE('',*,*,#14887,.T.);
#21006=ORIENTED_EDGE('',*,*,#14888,.T.);
#21007=ORIENTED_EDGE('',*,*,#14889,.F.);
#21008=ORIENTED_EDGE('',*,*,#14890,.T.);
#21009=ORIENTED_EDGE('',*,*,#14891,.T.);
#21010=ORIENTED_EDGE('',*,*,#14892,.T.);
#21011=ORIENTED_EDGE('',*,*,#14887,.F.);
#21012=ORIENTED_EDGE('',*,*,#14893,.T.);
#21013=ORIENTED_EDGE('',*,*,#14894,.T.);
#21014=ORIENTED_EDGE('',*,*,#14895,.T.);
#21015=ORIENTED_EDGE('',*,*,#14891,.F.);
#21016=ORIENTED_EDGE('',*,*,#14896,.T.);
#21017=ORIENTED_EDGE('',*,*,#14897,.T.);
#21018=ORIENTED_EDGE('',*,*,#14898,.T.);
#21019=ORIENTED_EDGE('',*,*,#14894,.F.);
#21020=ORIENTED_EDGE('',*,*,#14899,.T.);
#21021=ORIENTED_EDGE('',*,*,#14900,.T.);
#21022=ORIENTED_EDGE('',*,*,#14901,.T.);
#21023=ORIENTED_EDGE('',*,*,#14897,.F.);
#21024=ORIENTED_EDGE('',*,*,#14902,.T.);
#21025=ORIENTED_EDGE('',*,*,#14889,.T.);
#21026=ORIENTED_EDGE('',*,*,#14903,.T.);
#21027=ORIENTED_EDGE('',*,*,#14900,.F.);
#21028=ORIENTED_EDGE('',*,*,#14902,.F.);
#21029=ORIENTED_EDGE('',*,*,#14899,.F.);
#21030=ORIENTED_EDGE('',*,*,#14896,.F.);
#21031=ORIENTED_EDGE('',*,*,#14893,.F.);
#21032=ORIENTED_EDGE('',*,*,#14890,.F.);
#21033=ORIENTED_EDGE('',*,*,#14886,.F.);
#21034=ORIENTED_EDGE('',*,*,#14903,.F.);
#21035=ORIENTED_EDGE('',*,*,#14888,.F.);
#21036=ORIENTED_EDGE('',*,*,#14892,.F.);
#21037=ORIENTED_EDGE('',*,*,#14895,.F.);
#21038=ORIENTED_EDGE('',*,*,#14898,.F.);
#21039=ORIENTED_EDGE('',*,*,#14901,.F.);
#21648=CYLINDRICAL_SURFACE('',#26389,0.5);
#21649=CYLINDRICAL_SURFACE('',#26397,0.2942);
#22947=ADVANCED_FACE('',(#4166),#2858,.T.);
#22948=ADVANCED_FACE('',(#4167),#1492,.T.);
#22949=ADVANCED_FACE('',(#4168),#21648,.T.);
#22950=ADVANCED_FACE('',(#4169),#1493,.T.);
#22951=ADVANCED_FACE('',(#4170,#2295),#2859,.T.);
#22952=ADVANCED_FACE('',(#4171),#1494,.T.);
#22953=ADVANCED_FACE('',(#4172),#21649,.T.);
#22954=ADVANCED_FACE('',(#4173),#1495,.T.);
#22955=ADVANCED_FACE('',(#4174),#2860,.T.);
#22956=ADVANCED_FACE('',(#4175),#2861,.F.);
#22957=ADVANCED_FACE('',(#4176),#2862,.F.);
#22958=ADVANCED_FACE('',(#4177),#2863,.F.);
#22959=ADVANCED_FACE('',(#4178),#2864,.F.);
#22960=ADVANCED_FACE('',(#4179),#2865,.F.);
#22961=ADVANCED_FACE('',(#4180),#2866,.F.);
#22962=ADVANCED_FACE('',(#4181),#2867,.F.);
#22963=ADVANCED_FACE('',(#4182),#2868,.F.);
#23084=CLOSED_SHELL('',(#22947,#22948,#22949,#22950,#22951,#22952,#22953,
#22954,#22955));
#23085=CLOSED_SHELL('',(#22956,#22957,#22958,#22959,#22960,#22961,#22962,
#22963));
#26384=AXIS2_PLACEMENT_3D('',#62666,#32692,#32693);
#26385=AXIS2_PLACEMENT_3D('',#62667,#32694,#32695);
#26386=AXIS2_PLACEMENT_3D('',#62669,#32696,#32697);
#26387=AXIS2_PLACEMENT_3D('',#62670,#32698,#32699);
#26388=AXIS2_PLACEMENT_3D('',#62672,#32700,#32701);
#26389=AXIS2_PLACEMENT_3D('',#62674,#32703,#32704);
#26390=AXIS2_PLACEMENT_3D('',#62676,#32705,#32706);
#26391=AXIS2_PLACEMENT_3D('',#62678,#32708,#32709);
#26392=AXIS2_PLACEMENT_3D('',#62680,#32710,#32711);
#26393=AXIS2_PLACEMENT_3D('',#62682,#32713,#32714);
#26394=AXIS2_PLACEMENT_3D('',#62684,#32715,#32716);
#26395=AXIS2_PLACEMENT_3D('',#62685,#32717,#32718);
#26396=AXIS2_PLACEMENT_3D('',#62687,#32719,#32720);
#26397=AXIS2_PLACEMENT_3D('',#62689,#32722,#32723);
#26398=AXIS2_PLACEMENT_3D('',#62691,#32724,#32725);
#26399=AXIS2_PLACEMENT_3D('',#62693,#32727,#32728);
#26400=AXIS2_PLACEMENT_3D('',#62695,#32729,#32730);
#26401=AXIS2_PLACEMENT_3D('',#62697,#32732,#32733);
#26402=AXIS2_PLACEMENT_3D('',#62698,#32734,#32735);
#26403=AXIS2_PLACEMENT_3D('',#62707,#32740,#32741);
#26404=AXIS2_PLACEMENT_3D('',#62713,#32745,#32746);
#26405=AXIS2_PLACEMENT_3D('',#62719,#32750,#32751);
#26406=AXIS2_PLACEMENT_3D('',#62725,#32755,#32756);
#26407=AXIS2_PLACEMENT_3D('',#62731,#32760,#32761);
#26408=AXIS2_PLACEMENT_3D('',#62734,#32764,#32765);
#26409=AXIS2_PLACEMENT_3D('',#62735,#32766,#32767);
#32692=DIRECTION('axis',(0.,0.,1.));
#32693=DIRECTION('refdir',(1.,0.,0.));
#32694=DIRECTION('center_axis',(0.,1.,0.));
#32695=DIRECTION('ref_axis',(0.,0.,1.));
#32696=DIRECTION('center_axis',(0.,-1.,0.));
#32697=DIRECTION('ref_axis',(1.,0.,0.));
#32698=DIRECTION('center_axis',(0.,-1.,0.));
#32699=DIRECTION('ref_axis',(1.,0.,0.));
#32700=DIRECTION('center_axis',(0.,-1.,0.));
#32701=DIRECTION('ref_axis',(1.,0.,0.));
#32702=DIRECTION('',(0.707106781186548,0.707106781186547,8.65956056235494E-17));
#32703=DIRECTION('center_axis',(0.,-1.,0.));
#32704=DIRECTION('ref_axis',(1.,0.,0.));
#32705=DIRECTION('center_axis',(0.,-1.,0.));
#32706=DIRECTION('ref_axis',(1.,0.,0.));
#32707=DIRECTION('',(0.,1.,0.));
#32708=DIRECTION('center_axis',(0.,1.,0.));
#32709=DIRECTION('ref_axis',(1.,0.,0.));
#32710=DIRECTION('center_axis',(0.,-1.,0.));
#32711=DIRECTION('ref_axis',(1.,0.,0.));
#32712=DIRECTION('',(-0.707106781186547,0.707106781186548,-8.65956056235493E-17));
#32713=DIRECTION('center_axis',(0.,-1.,0.));
#32714=DIRECTION('ref_axis',(0.,0.,-1.));
#32715=DIRECTION('center_axis',(0.,-1.,0.));
#32716=DIRECTION('ref_axis',(1.,0.,0.));
#32717=DIRECTION('center_axis',(0.,1.,0.));
#32718=DIRECTION('ref_axis',(1.,0.,0.));
#32719=DIRECTION('center_axis',(0.,1.,0.));
#32720=DIRECTION('ref_axis',(1.,0.,0.));
#32721=DIRECTION('',(-0.447213595499958,0.894427190999916,-5.47678698264203E-17));
#32722=DIRECTION('center_axis',(0.,-1.,0.));
#32723=DIRECTION('ref_axis',(1.,0.,0.));
#32724=DIRECTION('center_axis',(0.,1.,0.));
#32725=DIRECTION('ref_axis',(1.,0.,0.));
#32726=DIRECTION('',(0.,1.,0.));
#32727=DIRECTION('center_axis',(0.,1.,0.));
#32728=DIRECTION('ref_axis',(1.,0.,0.));
#32729=DIRECTION('center_axis',(0.,-1.,0.));
#32730=DIRECTION('ref_axis',(1.,0.,0.));
#32731=DIRECTION('',(-0.707106781186547,0.707106781186548,-8.65956056235493E-17));
#32732=DIRECTION('center_axis',(0.,-1.,0.));
#32733=DIRECTION('ref_axis',(0.,0.,-1.));
#32734=DIRECTION('center_axis',(0.866025403784439,0.,-0.5));
#32735=DIRECTION('ref_axis',(0.5,0.,0.866025403784439));
#32736=DIRECTION('',(-0.5,0.,-0.866025403784439));
#32737=DIRECTION('',(0.,-1.,0.));
#32738=DIRECTION('',(0.5,0.,0.866025403784439));
#32739=DIRECTION('',(0.,-1.,0.));
#32740=DIRECTION('center_axis',(1.92296268638356E-16,0.,-1.));
#32741=DIRECTION('ref_axis',(1.,0.,1.92296268638356E-16));
#32742=DIRECTION('',(-1.,0.,-1.92296268638356E-16));
#32743=DIRECTION('',(0.,-1.,0.));
#32744=DIRECTION('',(1.,0.,1.92296268638356E-16));
#32745=DIRECTION('center_axis',(-0.866025403784439,0.,-0.5));
#32746=DIRECTION('ref_axis',(0.5,0.,-0.866025403784439));
#32747=DIRECTION('',(-0.5,0.,0.866025403784438));
#32748=DIRECTION('',(0.,-1.,0.));
#32749=DIRECTION('',(0.5,0.,-0.866025403784438));
#32750=DIRECTION('center_axis',(-0.866025403784439,0.,0.5));
#32751=DIRECTION('ref_axis',(-0.5,0.,-0.866025403784439));
#32752=DIRECTION('',(0.5,0.,0.866025403784439));
#32753=DIRECTION('',(0.,-1.,0.));
#32754=DIRECTION('',(-0.5,0.,-0.866025403784439));
#32755=DIRECTION('center_axis',(-1.92296268638356E-16,0.,1.));
#32756=DIRECTION('ref_axis',(-1.,0.,-1.92296268638356E-16));
#32757=DIRECTION('',(1.,0.,1.92296268638356E-16));
#32758=DIRECTION('',(0.,-1.,0.));
#32759=DIRECTION('',(-1.,0.,-1.92296268638356E-16));
#32760=DIRECTION('center_axis',(0.866025403784439,0.,0.5));
#32761=DIRECTION('ref_axis',(-0.5,0.,0.866025403784439));
#32762=DIRECTION('',(0.5,0.,-0.866025403784439));
#32763=DIRECTION('',(-0.5,0.,0.866025403784439));
#32764=DIRECTION('center_axis',(0.,1.,0.));
#32765=DIRECTION('ref_axis',(1.,0.,0.));
#32766=DIRECTION('center_axis',(0.,-1.,0.));
#32767=DIRECTION('ref_axis',(0.,0.,-1.));
#62666=CARTESIAN_POINT('',(0.,0.,0.));
#62667=CARTESIAN_POINT('Origin',(0.45,0.6,0.));
#62668=CARTESIAN_POINT('',(-0.45,0.6,-5.51091059616309E-17));
#62669=CARTESIAN_POINT('Origin',(0.,0.6,0.));
#62670=CARTESIAN_POINT('Origin',(0.,0.575,0.));
#62671=CARTESIAN_POINT('',(-0.5,0.55,-6.12323399573677E-17));
#62672=CARTESIAN_POINT('Origin',(0.,0.55,0.));
#62673=CARTESIAN_POINT('',(-0.475,0.575,-5.81707229594993E-17));
#62674=CARTESIAN_POINT('Origin',(0.,0.29,0.));
#62675=CARTESIAN_POINT('',(-0.5,0.0299999999999998,-6.12323399573677E-17));
#62676=CARTESIAN_POINT('Origin',(0.,0.0299999999999998,0.));
#62677=CARTESIAN_POINT('',(-0.5,0.29,-6.12323399573677E-17));
#62678=CARTESIAN_POINT('Origin',(0.,0.0150000000000001,0.));
#62679=CARTESIAN_POINT('',(-0.47,7.11236625150491E-17,-5.75583995599256E-17));
#62680=CARTESIAN_POINT('Origin',(0.,0.,0.));
#62681=CARTESIAN_POINT('',(-0.485,0.0150000000000001,-5.93953697586466E-17));
#62682=CARTESIAN_POINT('Origin',(0.32,0.,0.));
#62683=CARTESIAN_POINT('',(-0.32,-6.93889390390723E-18,-3.91886975727153E-17));
#62684=CARTESIAN_POINT('Origin',(0.,0.,0.));
#62685=CARTESIAN_POINT('Origin',(0.,-0.02,0.));
#62686=CARTESIAN_POINT('',(-0.2942,-0.0515999999999999,3.60291088309151E-17));
#62687=CARTESIAN_POINT('Origin',(0.,-0.0515999999999999,0.));
#62688=CARTESIAN_POINT('',(-0.31,-0.02,-3.7964050773568E-17));
#62689=CARTESIAN_POINT('Origin',(0.,-1.24,0.));
#62690=CARTESIAN_POINT('',(-0.2942,-2.4458,3.60291088309151E-17));
#62691=CARTESIAN_POINT('Origin',(0.,-2.4458,0.));
#62692=CARTESIAN_POINT('',(-0.2942,-1.24,-3.60291088309151E-17));
#62693=CARTESIAN_POINT('Origin',(0.,-2.47,0.));
#62694=CARTESIAN_POINT('',(-0.24,-2.5,-2.93915231795365E-17));
#62695=CARTESIAN_POINT('Origin',(0.,-2.5,0.));
#62696=CARTESIAN_POINT('',(-0.27,-2.47,-3.30654635769785E-17));
#62697=CARTESIAN_POINT('Origin',(0.,-2.5,0.));
#62698=CARTESIAN_POINT('Origin',(0.144337567297406,-0.6,-0.25));
#62699=CARTESIAN_POINT('',(0.288675134594813,-0.6,0.));
#62700=CARTESIAN_POINT('',(0.144337567297406,-0.6,-0.25));
#62701=CARTESIAN_POINT('',(0.288675134594813,-0.6,0.));
#62702=CARTESIAN_POINT('',(0.144337567297406,-0.96,-0.25));
#62703=CARTESIAN_POINT('',(0.144337567297406,-0.6,-0.25));
#62704=CARTESIAN_POINT('',(0.288675134594813,-0.96,0.));
#62705=CARTESIAN_POINT('',(0.288675134594813,-0.96,0.));
#62706=CARTESIAN_POINT('',(0.288675134594813,-0.6,0.));
#62707=CARTESIAN_POINT('Origin',(-0.144337567297406,-0.6,-0.25));
#62708=CARTESIAN_POINT('',(-0.144337567297406,-0.6,-0.25));
#62709=CARTESIAN_POINT('',(0.144337567297406,-0.6,-0.25));
#62710=CARTESIAN_POINT('',(-0.144337567297406,-0.96,-0.25));
#62711=CARTESIAN_POINT('',(-0.144337567297406,-0.6,-0.25));
#62712=CARTESIAN_POINT('',(0.144337567297406,-0.96,-0.25));
#62713=CARTESIAN_POINT('Origin',(-0.288675134594813,-0.6,-8.32667268468867E-17));
#62714=CARTESIAN_POINT('',(-0.288675134594813,-0.6,-3.53525079574969E-17));
#62715=CARTESIAN_POINT('',(-0.144337567297406,-0.6,-0.25));
#62716=CARTESIAN_POINT('',(-0.288675134594813,-0.96,-5.55111512312578E-17));
#62717=CARTESIAN_POINT('',(-0.288675134594813,-0.6,-3.53525079574969E-17));
#62718=CARTESIAN_POINT('',(-0.144337567297406,-0.96,-0.25));
#62719=CARTESIAN_POINT('Origin',(-0.144337567297407,-0.6,0.25));
#62720=CARTESIAN_POINT('',(-0.144337567297407,-0.6,0.25));
#62721=CARTESIAN_POINT('',(-0.288675134594813,-0.6,-3.53525079574969E-17));
#62722=CARTESIAN_POINT('',(-0.144337567297407,-0.96,0.25));
#62723=CARTESIAN_POINT('',(-0.144337567297407,-0.6,0.25));
#62724=CARTESIAN_POINT('',(-0.288675134594813,-0.96,-3.53525079574969E-17));
#62725=CARTESIAN_POINT('Origin',(0.144337567297406,-0.6,0.25));
#62726=CARTESIAN_POINT('',(0.144337567297406,-0.6,0.25));
#62727=CARTESIAN_POINT('',(-0.144337567297407,-0.6,0.25));
#62728=CARTESIAN_POINT('',(0.144337567297406,-0.96,0.25));
#62729=CARTESIAN_POINT('',(0.144337567297406,-0.6,0.25));
#62730=CARTESIAN_POINT('',(-0.144337567297407,-0.96,0.25));
#62731=CARTESIAN_POINT('Origin',(0.288675134594813,-0.6,0.));
#62732=CARTESIAN_POINT('',(0.144337567297406,-0.6,0.25));
#62733=CARTESIAN_POINT('',(0.144337567297406,-0.96,0.25));
#62734=CARTESIAN_POINT('Origin',(0.,-0.6,0.));
#62735=CARTESIAN_POINT('Origin',(0.,-0.96,0.));
#62884=UNCERTAINTY_MEASURE_WITH_UNIT(LENGTH_MEASURE(0.001),#62985,
'DISTANCE_ACCURACY_VALUE',
'Maximum model space distance between geometric entities at asserted c
onnectivities');
#62885=UNCERTAINTY_MEASURE_WITH_UNIT(LENGTH_MEASURE(0.001),#62985,
'DISTANCE_ACCURACY_VALUE',
'Maximum model space distance between geometric entities at asserted c
onnectivities');
#62983=(
GEOMETRIC_REPRESENTATION_CONTEXT(3)
GLOBAL_UNCERTAINTY_ASSIGNED_CONTEXT((#62884))
GLOBAL_UNIT_ASSIGNED_CONTEXT((#62985,#62987,#62988))
REPRESENTATION_CONTEXT('','3D')
);
#62984=(
GEOMETRIC_REPRESENTATION_CONTEXT(3)
GLOBAL_UNCERTAINTY_ASSIGNED_CONTEXT((#62885))
GLOBAL_UNIT_ASSIGNED_CONTEXT((#62985,#62987,#62988))
REPRESENTATION_CONTEXT('','3D')
);
#62985=(
LENGTH_UNIT()
NAMED_UNIT(*)
SI_UNIT(.CENTI.,.METRE.)
);
#62987=(
NAMED_UNIT(*)
PLANE_ANGLE_UNIT()
SI_UNIT($,.RADIAN.)
);
#62988=(
NAMED_UNIT(*)
SI_UNIT($,.STERADIAN.)
SOLID_ANGLE_UNIT()
);
#63086=SHAPE_DEFINITION_REPRESENTATION(#63297,#63446);
#63297=PRODUCT_DEFINITION_SHAPE('',$,#63545);
#63446=SHAPE_REPRESENTATION('',(#26384),#62983);
#63447=PRODUCT_DEFINITION_CONTEXT('part definition',#63743,'design');
#63545=PRODUCT_DEFINITION('Cap Screw - M6x25 (1)','Cap Screw - M6x25 (1)',
#63643,#63447);
#63643=PRODUCT_DEFINITION_FORMATION('',$,#63842);
#63743=APPLICATION_CONTEXT(
'Core Data for Automotive Mechanical Design Process');
#63744=PRODUCT_CONTEXT('part definition',#63743,'mechanical');
#63842=PRODUCT('Cap Screw - M6x25 (1)','Cap Screw - M6x25 (1)',
'Cap Screw - M6x25 (1)',(#63744));
#63913=COLOUR_RGB('Black',0.12,0.14,0.17);
#63914=FILL_AREA_STYLE_COLOUR('',#63913);
#63915=FILL_AREA_STYLE('',(#63914));
#63916=SURFACE_STYLE_FILL_AREA(#63915);
#63917=SURFACE_SIDE_STYLE('',(#63916));
#63918=SURFACE_STYLE_USAGE(.BOTH.,#63917);
#63919=PRESENTATION_STYLE_ASSIGNMENT((#63918));
ENDSEC;
END-ISO-10303-21;
